ISO-10303-21;
HEADER;
/* Generated by software containing ST-Developer
 * from STEP Tools, Inc. (www.steptools.com) 
 */

FILE_DESCRIPTION(
/* description */ (''),
/* implementation_level */ '2;1');

FILE_NAME(
/* name */ '12_Rear_Needle_Bearing_NK25-20.step',
/* time_stamp */ '2026-10-26T07:49:00-07:00',
/* author */ (''),
/* organization */ (''),
/* preprocessor_version */ 'ST-DEVELOPER v20.2',
/* originating_system */ 'Autodesk Translation Framework v15.15.0.0',
/* authorisation */ '');

FILE_SCHEMA (('AUTOMOTIVE_DESIGN { 1 0 10303 214 3 1 1 }'));
ENDSEC;

DATA;
#10=MECHANICAL_DESIGN_GEOMETRIC_PRESENTATION_REPRESENTATION('',(#185),#38507);
#155=SHAPE_REPRESENTATION_RELATIONSHIP('SRR','None',#38583,#170);
#170=ADVANCED_BREP_SHAPE_REPRESENTATION('',(#200),#38500);
#185=STYLED_ITEM('',(#38720),#200);
#200=MANIFOLD_SOLID_BREP('Body1',#15079);
#497=FACE_BOUND('',#3116,.T.);
#498=FACE_BOUND('',#3118,.T.);
#499=FACE_BOUND('',#3122,.T.);
#500=FACE_BOUND('',#3125,.T.);
#501=FACE_BOUND('',#3128,.T.);
#502=FACE_BOUND('',#3131,.T.);
#792=PLANE('',#16208);
#793=PLANE('',#16210);
#794=PLANE('',#16217);
#795=PLANE('',#16221);
#796=PLANE('',#16225);
#797=PLANE('',#16228);
#1496=CYLINDRICAL_SURFACE('',#16205,12.5);
#1497=CYLINDRICAL_SURFACE('',#16212,15.6);
#1498=CYLINDRICAL_SURFACE('',#16214,13.5);
#1499=CYLINDRICAL_SURFACE('',#16219,16.5);
#1500=CYLINDRICAL_SURFACE('',#16223,13.5);
#1501=CYLINDRICAL_SURFACE('',#16226,15.6);
#2147=FACE_OUTER_BOUND('',#3114,.T.);
#2148=FACE_OUTER_BOUND('',#3115,.T.);
#2149=FACE_OUTER_BOUND('',#3117,.T.);
#2150=FACE_OUTER_BOUND('',#3119,.T.);
#2151=FACE_OUTER_BOUND('',#3120,.T.);
#2152=FACE_OUTER_BOUND('',#3121,.T.);
#2153=FACE_OUTER_BOUND('',#3123,.T.);
#2154=FACE_OUTER_BOUND('',#3124,.T.);
#2155=FACE_OUTER_BOUND('',#3126,.T.);
#2156=FACE_OUTER_BOUND('',#3127,.T.);
#2157=FACE_OUTER_BOUND('',#3129,.T.);
#2158=FACE_OUTER_BOUND('',#3130,.T.);
#3114=EDGE_LOOP('',(#12409,#12410,#12411,#12412));
#3115=EDGE_LOOP('',(#12413));
#3116=EDGE_LOOP('',(#12414));
#3117=EDGE_LOOP('',(#12415));
#3118=EDGE_LOOP('',(#12416));
#3119=EDGE_LOOP('',(#12417,#12418,#12419,#12420));
#3120=EDGE_LOOP('',(#12421,#12422,#12423,#12424));
#3121=EDGE_LOOP('',(#12425));
#3122=EDGE_LOOP('',(#12426));
#3123=EDGE_LOOP('',(#12427,#12428,#12429,#12430));
#3124=EDGE_LOOP('',(#12431));
#3125=EDGE_LOOP('',(#12432));
#3126=EDGE_LOOP('',(#12433,#12434,#12435,#12436));
#3127=EDGE_LOOP('',(#12437));
#3128=EDGE_LOOP('',(#12438));
#3129=EDGE_LOOP('',(#12439,#12440,#12441,#12442));
#3130=EDGE_LOOP('',(#12443));
#3131=EDGE_LOOP('',(#12444));
#4116=LINE('',#26909,#5185);
#4117=LINE('',#26920,#5186);
#4118=LINE('',#26925,#5187);
#4119=LINE('',#26933,#5188);
#4120=LINE('',#26939,#5189);
#4121=LINE('',#26944,#5190);
#5185=VECTOR('',#19269,12.5);
#5186=VECTOR('',#19284,15.6);
#5187=VECTOR('',#19289,13.5);
#5188=VECTOR('',#19300,16.5);
#5189=VECTOR('',#19307,13.5);
#5190=VECTOR('',#19314,15.6);
#6089=CIRCLE('',#16206,12.5);
#6090=CIRCLE('',#16207,12.5);
#6091=CIRCLE('',#16209,15.6);
#6092=CIRCLE('',#16211,15.6);
#6093=CIRCLE('',#16213,15.6);
#6094=CIRCLE('',#16215,13.5);
#6095=CIRCLE('',#16216,13.5);
#6096=CIRCLE('',#16218,16.5);
#6097=CIRCLE('',#16220,16.5);
#6098=CIRCLE('',#16222,13.5);
#6099=CIRCLE('',#16224,13.5);
#6100=CIRCLE('',#16227,15.6);
#7094=VERTEX_POINT('',#26906);
#7095=VERTEX_POINT('',#26908);
#7096=VERTEX_POINT('',#26912);
#7097=VERTEX_POINT('',#26915);
#7098=VERTEX_POINT('',#26918);
#7099=VERTEX_POINT('',#26922);
#7100=VERTEX_POINT('',#26924);
#7101=VERTEX_POINT('',#26928);
#7102=VERTEX_POINT('',#26931);
#7103=VERTEX_POINT('',#26935);
#7104=VERTEX_POINT('',#26938);
#7105=VERTEX_POINT('',#26943);
#8953=EDGE_CURVE('',#7094,#7094,#6089,.T.);
#8954=EDGE_CURVE('',#7094,#7095,#4116,.T.);
#8955=EDGE_CURVE('',#7095,#7095,#6090,.T.);
#8956=EDGE_CURVE('',#7096,#7096,#6091,.T.);
#8957=EDGE_CURVE('',#7097,#7097,#6092,.T.);
#8958=EDGE_CURVE('',#7098,#7098,#6093,.T.);
#8959=EDGE_CURVE('',#7098,#7097,#4117,.T.);
#8960=EDGE_CURVE('',#7099,#7099,#6094,.T.);
#8961=EDGE_CURVE('',#7099,#7100,#4118,.T.);
#8962=EDGE_CURVE('',#7100,#7100,#6095,.T.);
#8963=EDGE_CURVE('',#7101,#7101,#6096,.T.);
#8964=EDGE_CURVE('',#7102,#7102,#6097,.T.);
#8965=EDGE_CURVE('',#7102,#7101,#4119,.T.);
#8966=EDGE_CURVE('',#7103,#7103,#6098,.T.);
#8967=EDGE_CURVE('',#7103,#7104,#4120,.T.);
#8968=EDGE_CURVE('',#7104,#7104,#6099,.T.);
#8969=EDGE_CURVE('',#7096,#7105,#4121,.T.);
#8970=EDGE_CURVE('',#7105,#7105,#6100,.T.);
#12409=ORIENTED_EDGE('',*,*,#8953,.T.);
#12410=ORIENTED_EDGE('',*,*,#8954,.T.);
#12411=ORIENTED_EDGE('',*,*,#8955,.F.);
#12412=ORIENTED_EDGE('',*,*,#8954,.F.);
#12413=ORIENTED_EDGE('',*,*,#8956,.F.);
#12414=ORIENTED_EDGE('',*,*,#8955,.T.);
#12415=ORIENTED_EDGE('',*,*,#8957,.F.);
#12416=ORIENTED_EDGE('',*,*,#8953,.F.);
#12417=ORIENTED_EDGE('',*,*,#8958,.T.);
#12418=ORIENTED_EDGE('',*,*,#8959,.T.);
#12419=ORIENTED_EDGE('',*,*,#8957,.T.);
#12420=ORIENTED_EDGE('',*,*,#8959,.F.);
#12421=ORIENTED_EDGE('',*,*,#8960,.T.);
#12422=ORIENTED_EDGE('',*,*,#8961,.T.);
#12423=ORIENTED_EDGE('',*,*,#8962,.F.);
#12424=ORIENTED_EDGE('',*,*,#8961,.F.);
#12425=ORIENTED_EDGE('',*,*,#8963,.F.);
#12426=ORIENTED_EDGE('',*,*,#8962,.T.);
#12427=ORIENTED_EDGE('',*,*,#8964,.F.);
#12428=ORIENTED_EDGE('',*,*,#8965,.T.);
#12429=ORIENTED_EDGE('',*,*,#8963,.T.);
#12430=ORIENTED_EDGE('',*,*,#8965,.F.);
#12431=ORIENTED_EDGE('',*,*,#8964,.T.);
#12432=ORIENTED_EDGE('',*,*,#8966,.F.);
#12433=ORIENTED_EDGE('',*,*,#8966,.T.);
#12434=ORIENTED_EDGE('',*,*,#8967,.T.);
#12435=ORIENTED_EDGE('',*,*,#8968,.F.);
#12436=ORIENTED_EDGE('',*,*,#8967,.F.);
#12437=ORIENTED_EDGE('',*,*,#8958,.F.);
#12438=ORIENTED_EDGE('',*,*,#8968,.T.);
#12439=ORIENTED_EDGE('',*,*,#8956,.T.);
#12440=ORIENTED_EDGE('',*,*,#8969,.T.);
#12441=ORIENTED_EDGE('',*,*,#8970,.F.);
#12442=ORIENTED_EDGE('',*,*,#8969,.F.);
#12443=ORIENTED_EDGE('',*,*,#8970,.T.);
#12444=ORIENTED_EDGE('',*,*,#8960,.F.);
#14714=ADVANCED_FACE('',(#2147),#1496,.F.);
#14715=ADVANCED_FACE('',(#2148,#497),#792,.T.);
#14716=ADVANCED_FACE('',(#2149,#498),#793,.T.);
#14717=ADVANCED_FACE('',(#2150),#1497,.F.);
#14718=ADVANCED_FACE('',(#2151),#1498,.F.);
#14719=ADVANCED_FACE('',(#2152,#499),#794,.T.);
#14720=ADVANCED_FACE('',(#2153),#1499,.T.);
#14721=ADVANCED_FACE('',(#2154,#500),#795,.T.);
#14722=ADVANCED_FACE('',(#2155),#1500,.F.);
#14723=ADVANCED_FACE('',(#2156,#501),#796,.T.);
#14724=ADVANCED_FACE('',(#2157),#1501,.F.);
#14725=ADVANCED_FACE('',(#2158,#502),#797,.T.);
#15079=CLOSED_SHELL('',(#14714,#14715,#14716,#14717,#14718,#14719,#14720,
#14721,#14722,#14723,#14724,#14725));
#16204=AXIS2_PLACEMENT_3D('',#26904,#19263,#19264);
#16205=AXIS2_PLACEMENT_3D('',#26905,#19265,#19266);
#16206=AXIS2_PLACEMENT_3D('',#26907,#19267,#19268);
#16207=AXIS2_PLACEMENT_3D('',#26910,#19270,#19271);
#16208=AXIS2_PLACEMENT_3D('',#26911,#19272,#19273);
#16209=AXIS2_PLACEMENT_3D('',#26913,#19274,#19275);
#16210=AXIS2_PLACEMENT_3D('',#26914,#19276,#19277);
#16211=AXIS2_PLACEMENT_3D('',#26916,#19278,#19279);
#16212=AXIS2_PLACEMENT_3D('',#26917,#19280,#19281);
#16213=AXIS2_PLACEMENT_3D('',#26919,#19282,#19283);
#16214=AXIS2_PLACEMENT_3D('',#26921,#19285,#19286);
#16215=AXIS2_PLACEMENT_3D('',#26923,#19287,#19288);
#16216=AXIS2_PLACEMENT_3D('',#26926,#19290,#19291);
#16217=AXIS2_PLACEMENT_3D('',#26927,#19292,#19293);
#16218=AXIS2_PLACEMENT_3D('',#26929,#19294,#19295);
#16219=AXIS2_PLACEMENT_3D('',#26930,#19296,#19297);
#16220=AXIS2_PLACEMENT_3D('',#26932,#19298,#19299);
#16221=AXIS2_PLACEMENT_3D('',#26934,#19301,#19302);
#16222=AXIS2_PLACEMENT_3D('',#26936,#19303,#19304);
#16223=AXIS2_PLACEMENT_3D('',#26937,#19305,#19306);
#16224=AXIS2_PLACEMENT_3D('',#26940,#19308,#19309);
#16225=AXIS2_PLACEMENT_3D('',#26941,#19310,#19311);
#16226=AXIS2_PLACEMENT_3D('',#26942,#19312,#19313);
#16227=AXIS2_PLACEMENT_3D('',#26945,#19315,#19316);
#16228=AXIS2_PLACEMENT_3D('',#26946,#19317,#19318);
#19263=DIRECTION('axis',(0.,0.,1.));
#19264=DIRECTION('refdir',(1.,0.,0.));
#19265=DIRECTION('center_axis',(1.,0.,0.));
#19266=DIRECTION('ref_axis',(0.,1.,0.));
#19267=DIRECTION('center_axis',(1.,0.,0.));
#19268=DIRECTION('ref_axis',(0.,0.,-1.));
#19269=DIRECTION('',(-1.,0.,0.));
#19270=DIRECTION('center_axis',(1.,0.,0.));
#19271=DIRECTION('ref_axis',(0.,0.,-1.));
#19272=DIRECTION('center_axis',(-1.,0.,0.));
#19273=DIRECTION('ref_axis',(0.,0.,1.));
#19274=DIRECTION('center_axis',(1.,0.,0.));
#19275=DIRECTION('ref_axis',(0.,1.,0.));
#19276=DIRECTION('center_axis',(1.,0.,0.));
#19277=DIRECTION('ref_axis',(0.,0.,-1.));
#19278=DIRECTION('center_axis',(-1.,0.,0.));
#19279=DIRECTION('ref_axis',(0.,1.,0.));
#19280=DIRECTION('center_axis',(1.,0.,0.));
#19281=DIRECTION('ref_axis',(0.,1.,0.));
#19282=DIRECTION('center_axis',(1.,0.,0.));
#19283=DIRECTION('ref_axis',(0.,0.,-1.));
#19284=DIRECTION('',(-1.,0.,0.));
#19285=DIRECTION('center_axis',(1.,0.,0.));
#19286=DIRECTION('ref_axis',(0.,1.,0.));
#19287=DIRECTION('center_axis',(1.,0.,0.));
#19288=DIRECTION('ref_axis',(0.,0.,-1.));
#19289=DIRECTION('',(-1.,0.,0.));
#19290=DIRECTION('center_axis',(1.,0.,0.));
#19291=DIRECTION('ref_axis',(0.,0.,-1.));
#19292=DIRECTION('center_axis',(-1.,0.,0.));
#19293=DIRECTION('ref_axis',(0.,0.,1.));
#19294=DIRECTION('center_axis',(1.,0.,0.));
#19295=DIRECTION('ref_axis',(0.,0.,-1.));
#19296=DIRECTION('center_axis',(1.,0.,0.));
#19297=DIRECTION('ref_axis',(0.,1.,0.));
#19298=DIRECTION('center_axis',(1.,0.,0.));
#19299=DIRECTION('ref_axis',(0.,0.,-1.));
#19300=DIRECTION('',(-1.,0.,0.));
#19301=DIRECTION('center_axis',(1.,0.,0.));
#19302=DIRECTION('ref_axis',(0.,0.,-1.));
#19303=DIRECTION('center_axis',(1.,0.,0.));
#19304=DIRECTION('ref_axis',(0.,0.,-1.));
#19305=DIRECTION('center_axis',(1.,0.,0.));
#19306=DIRECTION('ref_axis',(0.,1.,0.));
#19307=DIRECTION('',(-1.,0.,0.));
#19308=DIRECTION('center_axis',(1.,0.,0.));
#19309=DIRECTION('ref_axis',(0.,0.,-1.));
#19310=DIRECTION('center_axis',(-1.,0.,0.));
#19311=DIRECTION('ref_axis',(0.,0.,1.));
#19312=DIRECTION('center_axis',(1.,0.,0.));
#19313=DIRECTION('ref_axis',(0.,1.,0.));
#19314=DIRECTION('',(-1.,0.,0.));
#19315=DIRECTION('center_axis',(1.,0.,0.));
#19316=DIRECTION('ref_axis',(0.,0.,-1.));
#19317=DIRECTION('center_axis',(1.,0.,0.));
#19318=DIRECTION('ref_axis',(0.,0.,-1.));
#26904=CARTESIAN_POINT('',(0.,0.,0.));
#26905=CARTESIAN_POINT('Origin',(10.,0.,0.));
#26906=CARTESIAN_POINT('',(18.8,-12.5,-1.53080849893419E-15));
#26907=CARTESIAN_POINT('Origin',(18.8,0.,0.));
#26908=CARTESIAN_POINT('',(1.2,-12.5,-1.53080849893419E-15));
#26909=CARTESIAN_POINT('',(10.,-12.5,-1.53080849893419E-15));
#26910=CARTESIAN_POINT('Origin',(1.2,0.,0.));
#26911=CARTESIAN_POINT('Origin',(1.2,15.6,0.));
#26912=CARTESIAN_POINT('',(1.2,-15.6,-1.91044900666987E-15));
#26913=CARTESIAN_POINT('Origin',(1.2,0.,0.));
#26914=CARTESIAN_POINT('Origin',(18.8,12.5,0.));
#26915=CARTESIAN_POINT('',(18.8,-15.6,-1.91044900666987E-15));
#26916=CARTESIAN_POINT('Origin',(18.8,0.,0.));
#26917=CARTESIAN_POINT('Origin',(10.,0.,0.));
#26918=CARTESIAN_POINT('',(19.3,-15.6,-1.91044900666987E-15));
#26919=CARTESIAN_POINT('Origin',(19.3,0.,0.));
#26920=CARTESIAN_POINT('',(10.,-15.6,-1.91044900666987E-15));
#26921=CARTESIAN_POINT('Origin',(0.35,0.,0.));
#26922=CARTESIAN_POINT('',(0.7,-13.5,-1.65327317884893E-15));
#26923=CARTESIAN_POINT('Origin',(0.7,0.,0.));
#26924=CARTESIAN_POINT('',(0.,-13.5,-1.65327317884893E-15));
#26925=CARTESIAN_POINT('',(0.35,-13.5,-1.65327317884893E-15));
#26926=CARTESIAN_POINT('Origin',(0.,0.,0.));
#26927=CARTESIAN_POINT('Origin',(0.,16.5,0.));
#26928=CARTESIAN_POINT('',(0.,-16.5,-2.02066721859313E-15));
#26929=CARTESIAN_POINT('Origin',(0.,0.,0.));
#26930=CARTESIAN_POINT('Origin',(10.,0.,0.));
#26931=CARTESIAN_POINT('',(20.,-16.5,-2.02066721859313E-15));
#26932=CARTESIAN_POINT('Origin',(20.,0.,0.));
#26933=CARTESIAN_POINT('',(10.,-16.5,-2.02066721859313E-15));
#26934=CARTESIAN_POINT('Origin',(20.,13.5,0.));
#26935=CARTESIAN_POINT('',(20.,-13.5,-1.65327317884893E-15));
#26936=CARTESIAN_POINT('Origin',(20.,0.,0.));
#26937=CARTESIAN_POINT('Origin',(19.65,0.,0.));
#26938=CARTESIAN_POINT('',(19.3,-13.5,-1.65327317884893E-15));
#26939=CARTESIAN_POINT('',(19.65,-13.5,-1.65327317884893E-15));
#26940=CARTESIAN_POINT('Origin',(19.3,0.,0.));
#26941=CARTESIAN_POINT('Origin',(19.3,15.6,0.));
#26942=CARTESIAN_POINT('Origin',(10.,0.,0.));
#26943=CARTESIAN_POINT('',(0.7,-15.6,-1.91044900666987E-15));
#26944=CARTESIAN_POINT('',(10.,-15.6,-1.91044900666987E-15));
#26945=CARTESIAN_POINT('Origin',(0.7,0.,0.));
#26946=CARTESIAN_POINT('Origin',(0.7,13.5,0.));
#38483=UNCERTAINTY_MEASURE_WITH_UNIT(LENGTH_MEASURE(0.01),#38508,
'DISTANCE_ACCURACY_VALUE',
'Maximum model space distance between geometric entities at asserted c
onnectivities');
#38490=UNCERTAINTY_MEASURE_WITH_UNIT(LENGTH_MEASURE(0.01),#38508,
'DISTANCE_ACCURACY_VALUE',
'Maximum model space distance between geometric entities at asserted c
onnectivities');
#38500=(
GEOMETRIC_REPRESENTATION_CONTEXT(3)
GLOBAL_UNCERTAINTY_ASSIGNED_CONTEXT((#38483))
GLOBAL_UNIT_ASSIGNED_CONTEXT((#38508,#38510,#38511))
REPRESENTATION_CONTEXT('','3D')
);
#38507=(
GEOMETRIC_REPRESENTATION_CONTEXT(3)
GLOBAL_UNCERTAINTY_ASSIGNED_CONTEXT((#38490))
GLOBAL_UNIT_ASSIGNED_CONTEXT((#38508,#38510,#38511))
REPRESENTATION_CONTEXT('','3D')
);
#38508=(
LENGTH_UNIT()
NAMED_UNIT(*)
SI_UNIT(.MILLI.,.METRE.)
);
#38510=(
NAMED_UNIT(*)
PLANE_ANGLE_UNIT()
SI_UNIT($,.RADIAN.)
);
#38511=(
NAMED_UNIT(*)
SI_UNIT($,.STERADIAN.)
SOLID_ANGLE_UNIT()
);
#38521=SHAPE_DEFINITION_REPRESENTATION(#38537,#38583);
#38537=PRODUCT_DEFINITION_SHAPE('',$,#38600);
#38583=SHAPE_REPRESENTATION('',(#16204),#38500);
#38590=PRODUCT_DEFINITION_CONTEXT('part definition',#38640,'design');
#38600=PRODUCT_DEFINITION('2026-10-26-01-10-55-457',
'12_Rear_Needle_Bearing_NK25-20',#38616,#38590);
#38616=PRODUCT_DEFINITION_FORMATION('',$,#38651);
#38640=APPLICATION_CONTEXT(
'Core Data for Automotive Mechanical Design Process');
#38641=PRODUCT_CONTEXT('part definition',#38640,'mechanical');
#38651=PRODUCT('2026-10-26-01-10-55-457',
'12_Rear_Needle_Bearing_NK25-20',$,(#38641));
#38714=COLOUR_RGB('Grey',0.48,0.52,0.57);
#38715=FILL_AREA_STYLE_COLOUR('',#38714);
#38716=FILL_AREA_STYLE('',(#38715));
#38717=SURFACE_STYLE_FILL_AREA(#38716);
#38718=SURFACE_SIDE_STYLE('',(#38717));
#38719=SURFACE_STYLE_USAGE(.BOTH.,#38718);
#38720=PRESENTATION_STYLE_ASSIGNMENT((#38719));
ENDSEC;
END-ISO-10303-21;
